ISO-10303-21;
HEADER;
/* Generated by software containing ST-Developer
 * from STEP Tools, Inc. (www.steptools.com) 
 */

FILE_DESCRIPTION(
/* description */ (''),
/* implementation_level */ '2;1');

FILE_NAME(
/* name */ 'Nut_02.step',
/* time_stamp */ '2026-11-14T03:52:36-08:00',
/* author */ (''),
/* organization */ (''),
/* preprocessor_version */ 'ST-DEVELOPER v20.2',
/* originating_system */ 'Autodesk Translation Framework v15.17.0.0',
/* authorisation */ '');

FILE_SCHEMA (('AUTOMOTIVE_DESIGN { 1 0 10303 214 3 1 1 }'));
ENDSEC;

DATA;
#10=MECHANICAL_DESIGN_GEOMETRIC_PRESENTATION_REPRESENTATION('',(#198),#19443);
#182=SHAPE_REPRESENTATION_RELATIONSHIP('SRR','None',#19482,#190);
#190=ADVANCED_BREP_SHAPE_REPRESENTATION('',(#206),#19442);
#198=STYLED_ITEM('',(#19525),#206);
#206=MANIFOLD_SOLID_BREP('Body1',#2025);
#218=FACE_BOUND('',#475,.T.);
#219=FACE_BOUND('',#477,.T.);
#265=PLANE('',#2250);
#266=PLANE('',#2251);
#267=PLANE('',#2252);
#268=PLANE('',#2253);
#269=PLANE('',#2254);
#270=PLANE('',#2255);
#271=PLANE('',#2256);
#272=PLANE('',#2257);
#360=FACE_OUTER_BOUND('',#467,.T.);
#361=FACE_OUTER_BOUND('',#468,.T.);
#362=FACE_OUTER_BOUND('',#469,.T.);
#363=FACE_OUTER_BOUND('',#470,.T.);
#364=FACE_OUTER_BOUND('',#471,.T.);
#365=FACE_OUTER_BOUND('',#472,.T.);
#366=FACE_OUTER_BOUND('',#473,.T.);
#367=FACE_OUTER_BOUND('',#474,.T.);
#368=FACE_OUTER_BOUND('',#476,.T.);
#467=EDGE_LOOP('',(#1843,#1844,#1845,#1846));
#468=EDGE_LOOP('',(#1847,#1848,#1849,#1850));
#469=EDGE_LOOP('',(#1851,#1852,#1853,#1854));
#470=EDGE_LOOP('',(#1855,#1856,#1857,#1858));
#471=EDGE_LOOP('',(#1859,#1860,#1861,#1862));
#472=EDGE_LOOP('',(#1863,#1864,#1865,#1866));
#473=EDGE_LOOP('',(#1867,#1868,#1869,#1870));
#474=EDGE_LOOP('',(#1871,#1872,#1873,#1874,#1875,#1876));
#475=EDGE_LOOP('',(#1877));
#476=EDGE_LOOP('',(#1878,#1879,#1880,#1881,#1882,#1883));
#477=EDGE_LOOP('',(#1884));
#586=LINE('',#19376,#713);
#587=LINE('',#19381,#714);
#588=LINE('',#19383,#715);
#589=LINE('',#19385,#716);
#590=LINE('',#19386,#717);
#591=LINE('',#19389,#718);
#592=LINE('',#19391,#719);
#593=LINE('',#19392,#720);
#594=LINE('',#19395,#721);
#595=LINE('',#19397,#722);
#596=LINE('',#19398,#723);
#597=LINE('',#19401,#724);
#598=LINE('',#19403,#725);
#599=LINE('',#19404,#726);
#600=LINE('',#19407,#727);
#601=LINE('',#19409,#728);
#602=LINE('',#19410,#729);
#603=LINE('',#19412,#730);
#604=LINE('',#19413,#731);
#713=VECTOR('',#2642,3.933);
#714=VECTOR('',#2647,10.);
#715=VECTOR('',#2648,10.);
#716=VECTOR('',#2649,10.);
#717=VECTOR('',#2650,10.);
#718=VECTOR('',#2653,10.);
#719=VECTOR('',#2654,10.);
#720=VECTOR('',#2655,10.);
#721=VECTOR('',#2658,10.);
#722=VECTOR('',#2659,10.);
#723=VECTOR('',#2660,10.);
#724=VECTOR('',#2663,10.);
#725=VECTOR('',#2664,10.);
#726=VECTOR('',#2665,10.);
#727=VECTOR('',#2668,10.);
#728=VECTOR('',#2669,10.);
#729=VECTOR('',#2670,10.);
#730=VECTOR('',#2673,10.);
#731=VECTOR('',#2674,10.);
#774=CIRCLE('',#2248,3.933);
#775=CIRCLE('',#2249,3.933);
#980=VERTEX_POINT('',#19373);
#981=VERTEX_POINT('',#19375);
#982=VERTEX_POINT('',#19379);
#983=VERTEX_POINT('',#19380);
#984=VERTEX_POINT('',#19382);
#985=VERTEX_POINT('',#19384);
#986=VERTEX_POINT('',#19388);
#987=VERTEX_POINT('',#19390);
#988=VERTEX_POINT('',#19394);
#989=VERTEX_POINT('',#19396);
#990=VERTEX_POINT('',#19400);
#991=VERTEX_POINT('',#19402);
#992=VERTEX_POINT('',#19406);
#993=VERTEX_POINT('',#19408);
#1270=EDGE_CURVE('',#980,#980,#774,.T.);
#1271=EDGE_CURVE('',#980,#981,#586,.T.);
#1272=EDGE_CURVE('',#981,#981,#775,.T.);
#1273=EDGE_CURVE('',#982,#983,#587,.T.);
#1274=EDGE_CURVE('',#983,#984,#588,.T.);
#1275=EDGE_CURVE('',#985,#984,#589,.T.);
#1276=EDGE_CURVE('',#982,#985,#590,.T.);
#1277=EDGE_CURVE('',#986,#982,#591,.T.);
#1278=EDGE_CURVE('',#987,#985,#592,.T.);
#1279=EDGE_CURVE('',#986,#987,#593,.T.);
#1280=EDGE_CURVE('',#988,#986,#594,.T.);
#1281=EDGE_CURVE('',#989,#987,#595,.T.);
#1282=EDGE_CURVE('',#988,#989,#596,.T.);
#1283=EDGE_CURVE('',#990,#988,#597,.T.);
#1284=EDGE_CURVE('',#991,#989,#598,.T.);
#1285=EDGE_CURVE('',#990,#991,#599,.T.);
#1286=EDGE_CURVE('',#992,#990,#600,.T.);
#1287=EDGE_CURVE('',#993,#991,#601,.T.);
#1288=EDGE_CURVE('',#992,#993,#602,.T.);
#1289=EDGE_CURVE('',#983,#992,#603,.T.);
#1290=EDGE_CURVE('',#984,#993,#604,.T.);
#1843=ORIENTED_EDGE('',*,*,#1270,.T.);
#1844=ORIENTED_EDGE('',*,*,#1271,.T.);
#1845=ORIENTED_EDGE('',*,*,#1272,.F.);
#1846=ORIENTED_EDGE('',*,*,#1271,.F.);
#1847=ORIENTED_EDGE('',*,*,#1273,.T.);
#1848=ORIENTED_EDGE('',*,*,#1274,.T.);
#1849=ORIENTED_EDGE('',*,*,#1275,.F.);
#1850=ORIENTED_EDGE('',*,*,#1276,.F.);
#1851=ORIENTED_EDGE('',*,*,#1277,.T.);
#1852=ORIENTED_EDGE('',*,*,#1276,.T.);
#1853=ORIENTED_EDGE('',*,*,#1278,.F.);
#1854=ORIENTED_EDGE('',*,*,#1279,.F.);
#1855=ORIENTED_EDGE('',*,*,#1280,.T.);
#1856=ORIENTED_EDGE('',*,*,#1279,.T.);
#1857=ORIENTED_EDGE('',*,*,#1281,.F.);
#1858=ORIENTED_EDGE('',*,*,#1282,.F.);
#1859=ORIENTED_EDGE('',*,*,#1283,.T.);
#1860=ORIENTED_EDGE('',*,*,#1282,.T.);
#1861=ORIENTED_EDGE('',*,*,#1284,.F.);
#1862=ORIENTED_EDGE('',*,*,#1285,.F.);
#1863=ORIENTED_EDGE('',*,*,#1286,.T.);
#1864=ORIENTED_EDGE('',*,*,#1285,.T.);
#1865=ORIENTED_EDGE('',*,*,#1287,.F.);
#1866=ORIENTED_EDGE('',*,*,#1288,.F.);
#1867=ORIENTED_EDGE('',*,*,#1289,.T.);
#1868=ORIENTED_EDGE('',*,*,#1288,.T.);
#1869=ORIENTED_EDGE('',*,*,#1290,.F.);
#1870=ORIENTED_EDGE('',*,*,#1274,.F.);
#1871=ORIENTED_EDGE('',*,*,#1290,.T.);
#1872=ORIENTED_EDGE('',*,*,#1287,.T.);
#1873=ORIENTED_EDGE('',*,*,#1284,.T.);
#1874=ORIENTED_EDGE('',*,*,#1281,.T.);
#1875=ORIENTED_EDGE('',*,*,#1278,.T.);
#1876=ORIENTED_EDGE('',*,*,#1275,.T.);
#1877=ORIENTED_EDGE('',*,*,#1272,.T.);
#1878=ORIENTED_EDGE('',*,*,#1289,.F.);
#1879=ORIENTED_EDGE('',*,*,#1273,.F.);
#1880=ORIENTED_EDGE('',*,*,#1277,.F.);
#1881=ORIENTED_EDGE('',*,*,#1280,.F.);
#1882=ORIENTED_EDGE('',*,*,#1283,.F.);
#1883=ORIENTED_EDGE('',*,*,#1286,.F.);
#1884=ORIENTED_EDGE('',*,*,#1270,.F.);
#1921=CYLINDRICAL_SURFACE('',#2247,3.933);
#2009=ADVANCED_FACE('',(#360),#1921,.F.);
#2010=ADVANCED_FACE('',(#361),#265,.T.);
#2011=ADVANCED_FACE('',(#362),#266,.T.);
#2012=ADVANCED_FACE('',(#363),#267,.T.);
#2013=ADVANCED_FACE('',(#364),#268,.T.);
#2014=ADVANCED_FACE('',(#365),#269,.T.);
#2015=ADVANCED_FACE('',(#366),#270,.T.);
#2016=ADVANCED_FACE('',(#367,#218),#271,.T.);
#2017=ADVANCED_FACE('',(#368,#219),#272,.F.);
#2025=CLOSED_SHELL('',(#2009,#2010,#2011,#2012,#2013,#2014,#2015,#2016,
#2017));
#2246=AXIS2_PLACEMENT_3D('',#19371,#2636,#2637);
#2247=AXIS2_PLACEMENT_3D('',#19372,#2638,#2639);
#2248=AXIS2_PLACEMENT_3D('',#19374,#2640,#2641);
#2249=AXIS2_PLACEMENT_3D('',#19377,#2643,#2644);
#2250=AXIS2_PLACEMENT_3D('',#19378,#2645,#2646);
#2251=AXIS2_PLACEMENT_3D('',#19387,#2651,#2652);
#2252=AXIS2_PLACEMENT_3D('',#19393,#2656,#2657);
#2253=AXIS2_PLACEMENT_3D('',#19399,#2661,#2662);
#2254=AXIS2_PLACEMENT_3D('',#19405,#2666,#2667);
#2255=AXIS2_PLACEMENT_3D('',#19411,#2671,#2672);
#2256=AXIS2_PLACEMENT_3D('',#19414,#2675,#2676);
#2257=AXIS2_PLACEMENT_3D('',#19415,#2677,#2678);
#2636=DIRECTION('axis',(0.,0.,1.));
#2637=DIRECTION('refdir',(1.,0.,0.));
#2638=DIRECTION('center_axis',(0.,0.,-1.));
#2639=DIRECTION('ref_axis',(1.,0.,0.));
#2640=DIRECTION('center_axis',(0.,0.,1.));
#2641=DIRECTION('ref_axis',(1.,0.,0.));
#2642=DIRECTION('',(0.,0.,-1.));
#2643=DIRECTION('center_axis',(0.,0.,1.));
#2644=DIRECTION('ref_axis',(1.,0.,0.));
#2645=DIRECTION('center_axis',(-0.866025403784439,0.499999999999999,0.));
#2646=DIRECTION('ref_axis',(0.499999999999999,0.866025403784439,0.));
#2647=DIRECTION('',(0.499999999999999,0.866025403784439,0.));
#2648=DIRECTION('',(0.,0.,-1.));
#2649=DIRECTION('',(0.499999999999999,0.866025403784439,0.));
#2650=DIRECTION('',(0.,0.,-1.));
#2651=DIRECTION('center_axis',(-0.866025403784438,-0.500000000000001,0.));
#2652=DIRECTION('ref_axis',(-0.500000000000001,0.866025403784438,0.));
#2653=DIRECTION('',(-0.500000000000001,0.866025403784438,0.));
#2654=DIRECTION('',(-0.500000000000001,0.866025403784438,0.));
#2655=DIRECTION('',(0.,0.,-1.));
#2656=DIRECTION('center_axis',(4.93050094494016E-16,-1.,0.));
#2657=DIRECTION('ref_axis',(-1.,-4.93050094494016E-16,0.));
#2658=DIRECTION('',(-1.,-4.93050094494016E-16,0.));
#2659=DIRECTION('',(-1.,-4.93050094494016E-16,0.));
#2660=DIRECTION('',(0.,0.,-1.));
#2661=DIRECTION('center_axis',(0.866025403784439,-0.5,0.));
#2662=DIRECTION('ref_axis',(-0.5,-0.866025403784439,0.));
#2663=DIRECTION('',(-0.5,-0.866025403784439,0.));
#2664=DIRECTION('',(-0.5,-0.866025403784439,0.));
#2665=DIRECTION('',(0.,0.,-1.));
#2666=DIRECTION('center_axis',(0.866025403784439,0.5,0.));
#2667=DIRECTION('ref_axis',(0.5,-0.866025403784439,0.));
#2668=DIRECTION('',(0.5,-0.866025403784439,0.));
#2669=DIRECTION('',(0.5,-0.866025403784439,0.));
#2670=DIRECTION('',(0.,0.,-1.));
#2671=DIRECTION('center_axis',(-6.57400125992021E-16,1.,0.));
#2672=DIRECTION('ref_axis',(1.,6.57400125992021E-16,0.));
#2673=DIRECTION('',(1.,6.57400125992021E-16,0.));
#2674=DIRECTION('',(1.,6.57400125992021E-16,0.));
#2675=DIRECTION('center_axis',(0.,0.,-1.));
#2676=DIRECTION('ref_axis',(1.,0.,0.));
#2677=DIRECTION('center_axis',(0.,0.,-1.));
#2678=DIRECTION('ref_axis',(1.,0.,0.));
#19371=CARTESIAN_POINT('',(0.,0.,0.));
#19372=CARTESIAN_POINT('Origin',(0.,0.,307.));
#19373=CARTESIAN_POINT('',(-3.933,4.81653586104654E-16,307.));
#19374=CARTESIAN_POINT('Origin',(0.,0.,307.));
#19375=CARTESIAN_POINT('',(-3.933,4.81653586104654E-16,302.));
#19376=CARTESIAN_POINT('',(-3.933,4.81653586104654E-16,307.));
#19377=CARTESIAN_POINT('Origin',(0.,0.,302.));
#19378=CARTESIAN_POINT('Origin',(-6.75523463248397,-4.9960036108132E-15,
307.));
#19379=CARTESIAN_POINT('',(-6.75523463248397,-4.9960036108132E-15,307.));
#19380=CARTESIAN_POINT('',(-3.37761731624199,5.85020480025555,307.));
#19381=CARTESIAN_POINT('',(-6.75523463248397,-4.9960036108132E-15,307.));
#19382=CARTESIAN_POINT('',(-3.37761731624199,5.85020480025555,302.));
#19383=CARTESIAN_POINT('',(-3.37761731624199,5.85020480025555,307.));
#19384=CARTESIAN_POINT('',(-6.75523463248397,-4.9960036108132E-15,302.));
#19385=CARTESIAN_POINT('',(-6.75523463248397,-4.9960036108132E-15,302.));
#19386=CARTESIAN_POINT('',(-6.75523463248397,-4.9960036108132E-15,307.));
#19387=CARTESIAN_POINT('Origin',(-3.37761731624198,-5.85020480025556,307.));
#19388=CARTESIAN_POINT('',(-3.37761731624198,-5.85020480025556,307.));
#19389=CARTESIAN_POINT('',(-3.37761731624198,-5.85020480025556,307.));
#19390=CARTESIAN_POINT('',(-3.37761731624198,-5.85020480025556,302.));
#19391=CARTESIAN_POINT('',(-3.37761731624198,-5.85020480025556,302.));
#19392=CARTESIAN_POINT('',(-3.37761731624198,-5.85020480025556,307.));
#19393=CARTESIAN_POINT('Origin',(3.37761731624199,-5.85020480025555,307.));
#19394=CARTESIAN_POINT('',(3.37761731624199,-5.85020480025555,307.));
#19395=CARTESIAN_POINT('',(3.37761731624199,-5.85020480025555,307.));
#19396=CARTESIAN_POINT('',(3.37761731624199,-5.85020480025555,302.));
#19397=CARTESIAN_POINT('',(3.37761731624199,-5.85020480025555,302.));
#19398=CARTESIAN_POINT('',(3.37761731624199,-5.85020480025555,307.));
#19399=CARTESIAN_POINT('Origin',(6.75523463248397,2.77555756156289E-15,
307.));
#19400=CARTESIAN_POINT('',(6.75523463248397,2.77555756156289E-15,307.));
#19401=CARTESIAN_POINT('',(6.75523463248397,2.77555756156289E-15,307.));
#19402=CARTESIAN_POINT('',(6.75523463248397,2.77555756156289E-15,302.));
#19403=CARTESIAN_POINT('',(6.75523463248397,2.77555756156289E-15,302.));
#19404=CARTESIAN_POINT('',(6.75523463248397,2.77555756156289E-15,307.));
#19405=CARTESIAN_POINT('Origin',(3.37761731624198,5.85020480025556,307.));
#19406=CARTESIAN_POINT('',(3.37761731624198,5.85020480025556,307.));
#19407=CARTESIAN_POINT('',(3.37761731624198,5.85020480025556,307.));
#19408=CARTESIAN_POINT('',(3.37761731624198,5.85020480025556,302.));
#19409=CARTESIAN_POINT('',(3.37761731624198,5.85020480025556,302.));
#19410=CARTESIAN_POINT('',(3.37761731624198,5.85020480025556,307.));
#19411=CARTESIAN_POINT('Origin',(-3.37761731624199,5.85020480025555,307.));
#19412=CARTESIAN_POINT('',(-3.37761731624199,5.85020480025555,307.));
#19413=CARTESIAN_POINT('',(-3.37761731624199,5.85020480025555,302.));
#19414=CARTESIAN_POINT('Origin',(0.,0.,302.));
#19415=CARTESIAN_POINT('Origin',(0.,0.,307.));
#19432=UNCERTAINTY_MEASURE_WITH_UNIT(LENGTH_MEASURE(0.01),#19444,
'DISTANCE_ACCURACY_VALUE',
'Maximum model space distance between geometric entities at asserted c
onnectivities');
#19433=UNCERTAINTY_MEASURE_WITH_UNIT(LENGTH_MEASURE(0.01),#19444,
'DISTANCE_ACCURACY_VALUE',
'Maximum model space distance between geometric entities at asserted c
onnectivities');
#19442=(
GEOMETRIC_REPRESENTATION_CONTEXT(3)
GLOBAL_UNCERTAINTY_ASSIGNED_CONTEXT((#19432))
GLOBAL_UNIT_ASSIGNED_CONTEXT((#19444,#19446,#19447))
REPRESENTATION_CONTEXT('','3D')
);
#19443=(
GEOMETRIC_REPRESENTATION_CONTEXT(3)
GLOBAL_UNCERTAINTY_ASSIGNED_CONTEXT((#19433))
GLOBAL_UNIT_ASSIGNED_CONTEXT((#19444,#19446,#19447))
REPRESENTATION_CONTEXT('','3D')
);
#19444=(
LENGTH_UNIT()
NAMED_UNIT(*)
SI_UNIT(.MILLI.,.METRE.)
);
#19446=(
NAMED_UNIT(*)
PLANE_ANGLE_UNIT()
SI_UNIT($,.RADIAN.)
);
#19447=(
NAMED_UNIT(*)
SI_UNIT($,.STERADIAN.)
SOLID_ANGLE_UNIT()
);
#19456=SHAPE_DEFINITION_REPRESENTATION(#19465,#19482);
#19465=PRODUCT_DEFINITION_SHAPE('',$,#19492);
#19482=SHAPE_REPRESENTATION('',(#2246),#19442);
#19483=PRODUCT_DEFINITION_CONTEXT('part definition',#19512,'design');
#19492=PRODUCT_DEFINITION('Nut_02','Nut_02',#19501,#19483);
#19501=PRODUCT_DEFINITION_FORMATION('',$,#19522);
#19512=APPLICATION_CONTEXT(
'Core Data for Automotive Mechanical Design Process');
#19513=PRODUCT_CONTEXT('part definition',#19512,'mechanical');
#19522=PRODUCT('Nut_02','Nut_02',$,(#19513));
#19525=PRESENTATION_STYLE_ASSIGNMENT((#19528));
#19528=SURFACE_STYLE_USAGE(.BOTH.,#19531);
#19531=SURFACE_SIDE_STYLE('',(#19534));
#19534=SURFACE_STYLE_FILL_AREA(#19537);
#19537=FILL_AREA_STYLE('Opaque(160,160,160)',(#19540));
#19540=FILL_AREA_STYLE_COLOUR('Opaque(160,160,160)',#19543);
#19543=COLOUR_RGB('Opaque(160,160,160)',0.627450980392157,0.627450980392157,
0.627450980392157);
ENDSEC;
END-ISO-10303-21;
